ISO-10303-21;
HEADER;
/* Generated by software containing ST-Developer
 * from STEP Tools, Inc. (www.steptools.com) 
 */

FILE_DESCRIPTION(
/* description */ ('Shaft runout checking stand'),
/* implementation_level */ '2;1');

FILE_NAME(
/* name */ 'Axle keeper (1).step',
/* time_stamp */ '2026-11-02T21:12:33-08:00',
/* author */ (''),
/* organization */ (''),
/* preprocessor_version */ 'ST-DEVELOPER v20.2',
/* originating_system */ 'Autodesk Translation Framework v15.17.0.0',
/* authorisation */ '');

FILE_SCHEMA (('AUTOMOTIVE_DESIGN { 1 0 10303 214 3 1 1 }'));
ENDSEC;

DATA;
#10=MECHANICAL_DESIGN_GEOMETRIC_PRESENTATION_REPRESENTATION('',(#476),#11748);
#390=SHAPE_REPRESENTATION_RELATIONSHIP('SRR','None',#11939,#433);
#433=ADVANCED_BREP_SHAPE_REPRESENTATION('',(#527),#11715);
#476=STYLED_ITEM('',(#12169),#527);
#527=MANIFOLD_SOLID_BREP('Body1',#6219);
#611=FACE_BOUND('',#1598,.T.);
#612=FACE_BOUND('',#1600,.T.);
#746=CIRCLE('',#6966,0.225);
#747=CIRCLE('',#6967,0.225);
#748=CIRCLE('',#6969,0.8);
#749=CIRCLE('',#6970,0.8);
#973=CYLINDRICAL_SURFACE('',#6965,0.225);
#974=CYLINDRICAL_SURFACE('',#6968,0.8);
#1178=FACE_OUTER_BOUND('',#1595,.T.);
#1179=FACE_OUTER_BOUND('',#1596,.T.);
#1180=FACE_OUTER_BOUND('',#1597,.T.);
#1181=FACE_OUTER_BOUND('',#1599,.T.);
#1595=EDGE_LOOP('',(#4752,#4753,#4754,#4755));
#1596=EDGE_LOOP('',(#4756,#4757,#4758,#4759));
#1597=EDGE_LOOP('',(#4760));
#1598=EDGE_LOOP('',(#4761));
#1599=EDGE_LOOP('',(#4762));
#1600=EDGE_LOOP('',(#4763));
#2142=LINE('',#10188,#2609);
#2143=LINE('',#10194,#2610);
#2609=VECTOR('',#8215,0.225);
#2610=VECTOR('',#8222,0.8);
#3040=VERTEX_POINT('',#10185);
#3041=VERTEX_POINT('',#10187);
#3042=VERTEX_POINT('',#10191);
#3043=VERTEX_POINT('',#10193);
#3662=EDGE_CURVE('',#3040,#3040,#746,.T.);
#3663=EDGE_CURVE('',#3040,#3041,#2142,.T.);
#3664=EDGE_CURVE('',#3041,#3041,#747,.T.);
#3665=EDGE_CURVE('',#3042,#3042,#748,.T.);
#3666=EDGE_CURVE('',#3042,#3043,#2143,.T.);
#3667=EDGE_CURVE('',#3043,#3043,#749,.T.);
#4752=ORIENTED_EDGE('',*,*,#3662,.F.);
#4753=ORIENTED_EDGE('',*,*,#3663,.T.);
#4754=ORIENTED_EDGE('',*,*,#3664,.T.);
#4755=ORIENTED_EDGE('',*,*,#3663,.F.);
#4756=ORIENTED_EDGE('',*,*,#3665,.F.);
#4757=ORIENTED_EDGE('',*,*,#3666,.T.);
#4758=ORIENTED_EDGE('',*,*,#3667,.T.);
#4759=ORIENTED_EDGE('',*,*,#3666,.F.);
#4760=ORIENTED_EDGE('',*,*,#3665,.T.);
#4761=ORIENTED_EDGE('',*,*,#3662,.T.);
#4762=ORIENTED_EDGE('',*,*,#3667,.F.);
#4763=ORIENTED_EDGE('',*,*,#3664,.F.);
#5708=PLANE('',#6971);
#5709=PLANE('',#6972);
#5978=ADVANCED_FACE('',(#1178),#973,.F.);
#5979=ADVANCED_FACE('',(#1179),#974,.T.);
#5980=ADVANCED_FACE('',(#1180,#611),#5708,.T.);
#5981=ADVANCED_FACE('',(#1181,#612),#5709,.F.);
#6219=CLOSED_SHELL('',(#5978,#5979,#5980,#5981));
#6964=AXIS2_PLACEMENT_3D('',#10183,#8209,#8210);
#6965=AXIS2_PLACEMENT_3D('',#10184,#8211,#8212);
#6966=AXIS2_PLACEMENT_3D('',#10186,#8213,#8214);
#6967=AXIS2_PLACEMENT_3D('',#10189,#8216,#8217);
#6968=AXIS2_PLACEMENT_3D('',#10190,#8218,#8219);
#6969=AXIS2_PLACEMENT_3D('',#10192,#8220,#8221);
#6970=AXIS2_PLACEMENT_3D('',#10195,#8223,#8224);
#6971=AXIS2_PLACEMENT_3D('',#10196,#8225,#8226);
#6972=AXIS2_PLACEMENT_3D('',#10197,#8227,#8228);
#8209=DIRECTION('axis',(0.,0.,1.));
#8210=DIRECTION('refdir',(1.,0.,0.));
#8211=DIRECTION('center_axis',(0.,1.,0.));
#8212=DIRECTION('ref_axis',(1.,0.,0.));
#8213=DIRECTION('center_axis',(0.,-1.,0.));
#8214=DIRECTION('ref_axis',(1.,0.,0.));
#8215=DIRECTION('',(0.,-1.,0.));
#8216=DIRECTION('center_axis',(0.,-1.,0.));
#8217=DIRECTION('ref_axis',(1.,0.,0.));
#8218=DIRECTION('center_axis',(0.,1.,0.));
#8219=DIRECTION('ref_axis',(1.,0.,0.));
#8220=DIRECTION('center_axis',(0.,1.,0.));
#8221=DIRECTION('ref_axis',(1.,0.,0.));
#8222=DIRECTION('',(0.,-1.,0.));
#8223=DIRECTION('center_axis',(0.,1.,0.));
#8224=DIRECTION('ref_axis',(1.,0.,0.));
#8225=DIRECTION('center_axis',(0.,1.,0.));
#8226=DIRECTION('ref_axis',(1.,0.,0.));
#8227=DIRECTION('center_axis',(0.,1.,0.));
#8228=DIRECTION('ref_axis',(1.,0.,0.));
#10183=CARTESIAN_POINT('',(0.,0.,0.));
#10184=CARTESIAN_POINT('Origin',(2.,-9.2,5.));
#10185=CARTESIAN_POINT('',(1.775,-9.,5.));
#10186=CARTESIAN_POINT('Origin',(2.,-9.,5.));
#10187=CARTESIAN_POINT('',(1.775,-9.2,5.));
#10188=CARTESIAN_POINT('',(1.775,-9.2,5.));
#10189=CARTESIAN_POINT('Origin',(2.,-9.2,5.));
#10190=CARTESIAN_POINT('Origin',(2.,-9.2,5.));
#10191=CARTESIAN_POINT('',(1.2,-9.,5.));
#10192=CARTESIAN_POINT('Origin',(2.,-9.,5.));
#10193=CARTESIAN_POINT('',(1.2,-9.2,5.));
#10194=CARTESIAN_POINT('',(1.2,-9.2,5.));
#10195=CARTESIAN_POINT('Origin',(2.,-9.2,5.));
#10196=CARTESIAN_POINT('Origin',(2.,-9.,5.));
#10197=CARTESIAN_POINT('Origin',(2.,-9.2,5.));
#11666=UNCERTAINTY_MEASURE_WITH_UNIT(LENGTH_MEASURE(0.001),#11749,
'DISTANCE_ACCURACY_VALUE',
'Maximum model space distance between geometric entities at asserted c
onnectivities');
#11699=UNCERTAINTY_MEASURE_WITH_UNIT(LENGTH_MEASURE(0.001),#11749,
'DISTANCE_ACCURACY_VALUE',
'Maximum model space distance between geometric entities at asserted c
onnectivities');
#11715=(
GEOMETRIC_REPRESENTATION_CONTEXT(3)
GLOBAL_UNCERTAINTY_ASSIGNED_CONTEXT((#11666))
GLOBAL_UNIT_ASSIGNED_CONTEXT((#11749,#11751,#11752))
REPRESENTATION_CONTEXT('','3D')
);
#11748=(
GEOMETRIC_REPRESENTATION_CONTEXT(3)
GLOBAL_UNCERTAINTY_ASSIGNED_CONTEXT((#11699))
GLOBAL_UNIT_ASSIGNED_CONTEXT((#11749,#11751,#11752))
REPRESENTATION_CONTEXT('','3D')
);
#11749=(
LENGTH_UNIT()
NAMED_UNIT(*)
SI_UNIT(.CENTI.,.METRE.)
);
#11751=(
NAMED_UNIT(*)
PLANE_ANGLE_UNIT()
SI_UNIT($,.RADIAN.)
);
#11752=(
NAMED_UNIT(*)
SI_UNIT($,.STERADIAN.)
SOLID_ANGLE_UNIT()
);
#11768=SHAPE_DEFINITION_REPRESENTATION(#11816,#11939);
#11816=PRODUCT_DEFINITION_SHAPE('',$,#11988);
#11939=SHAPE_REPRESENTATION('',(#6964),#11715);
#11972=PRODUCT_DEFINITION_CONTEXT('part definition',#12118,'design');
#11988=PRODUCT_DEFINITION('Axle keeper_1','Axle keeper (1)',#12036,#11972);
#12036=PRODUCT_DEFINITION_FORMATION('',$,#12135);
#12118=APPLICATION_CONTEXT(
'Core Data for Automotive Mechanical Design Process');
#12119=PRODUCT_CONTEXT('part definition',#12118,'mechanical');
#12135=PRODUCT('Axle keeper_1','Axle keeper (1)','Axle keeper',(#12119));
#12169=PRESENTATION_STYLE_ASSIGNMENT((#12174));
#12174=SURFACE_STYLE_USAGE(.BOTH.,#12179);
#12179=SURFACE_SIDE_STYLE('',(#12184));
#12184=SURFACE_STYLE_FILL_AREA(#12189);
#12189=FILL_AREA_STYLE('CAD Library Painted - Engineering blue',(#12194));
#12194=FILL_AREA_STYLE_COLOUR('CAD Library Painted - Engineering blue',
#12199);
#12199=COLOUR_RGB('CAD Library Painted - Engineering blue',0.12156862745098,
0.356862745098039,0.6);
ENDSEC;
END-ISO-10303-21;
